ISO-10303-21;
HEADER;
/* Generated by software containing ST-Developer
 * from STEP Tools, Inc. (www.steptools.com) 
 */

FILE_DESCRIPTION(
/* description */ ('Lifting hook block with sheave'),
/* implementation_level */ '2;1');

FILE_NAME(
/* name */ 'M8x75 cross bolt.step',
/* time_stamp */ '2026-10-28T03:23:54-07:00',
/* author */ (''),
/* organization */ (''),
/* preprocessor_version */ 'ST-DEVELOPER v20.2',
/* originating_system */ 'Autodesk Translation Framework v15.17.0.0',
/* authorisation */ '');

FILE_SCHEMA (('AUTOMOTIVE_DESIGN { 1 0 10303 214 3 1 1 }'));
ENDSEC;

DATA;
#10=MECHANICAL_DESIGN_GEOMETRIC_PRESENTATION_REPRESENTATION('',(#363),#9391);
#267=CONICAL_SURFACE('',#5500,0.625,0.785398163397448);
#268=CONICAL_SURFACE('',#5504,0.635,0.785398163397449);
#269=CONICAL_SURFACE('',#5508,0.41,0.463647609000806);
#285=ORIENTED_CLOSED_SHELL('',*,#4899,.F.);
#288=BREP_WITH_VOIDS('Body1',#4900,(#285));
#303=SHAPE_REPRESENTATION_RELATIONSHIP('SRR','None',#9534,#333);
#333=ADVANCED_BREP_SHAPE_REPRESENTATION('',(#288),#9369);
#363=STYLED_ITEM('',(#9766),#288);
#540=LINE('',#8053,#828);
#541=LINE('',#8055,#829);
#542=LINE('',#8057,#830);
#543=LINE('',#8058,#831);
#544=LINE('',#8061,#832);
#545=LINE('',#8063,#833);
#546=LINE('',#8064,#834);
#547=LINE('',#8067,#835);
#548=LINE('',#8069,#836);
#549=LINE('',#8070,#837);
#550=LINE('',#8073,#838);
#551=LINE('',#8075,#839);
#552=LINE('',#8076,#840);
#553=LINE('',#8079,#841);
#554=LINE('',#8081,#842);
#555=LINE('',#8082,#843);
#556=LINE('',#8084,#844);
#557=LINE('',#8085,#845);
#558=LINE('',#8095,#846);
#559=LINE('',#8104,#847);
#560=LINE('',#8108,#848);
#561=LINE('',#8112,#849);
#562=LINE('',#8119,#850);
#563=LINE('',#8121,#851);
#828=VECTOR('',#6497,1.);
#829=VECTOR('',#6498,1.);
#830=VECTOR('',#6499,1.);
#831=VECTOR('',#6500,1.);
#832=VECTOR('',#6503,1.);
#833=VECTOR('',#6504,1.);
#834=VECTOR('',#6505,1.);
#835=VECTOR('',#6508,1.);
#836=VECTOR('',#6509,1.);
#837=VECTOR('',#6510,1.);
#838=VECTOR('',#6513,1.);
#839=VECTOR('',#6514,1.);
#840=VECTOR('',#6515,1.);
#841=VECTOR('',#6518,1.);
#842=VECTOR('',#6519,1.);
#843=VECTOR('',#6520,1.);
#844=VECTOR('',#6523,1.);
#845=VECTOR('',#6524,1.);
#846=VECTOR('',#6537,0.4);
#847=VECTOR('',#6550,0.625);
#848=VECTOR('',#6555,0.65);
#849=VECTOR('',#6560,0.635);
#850=VECTOR('',#6569,0.41);
#851=VECTOR('',#6572,0.4);
#1048=CYLINDRICAL_SURFACE('',#5495,0.4);
#1049=CYLINDRICAL_SURFACE('',#5502,0.65);
#1050=CYLINDRICAL_SURFACE('',#5510,0.3933);
#1159=FACE_BOUND('',#1670,.T.);
#1160=FACE_BOUND('',#1678,.T.);
#1320=FACE_OUTER_BOUND('',#1661,.T.);
#1321=FACE_OUTER_BOUND('',#1662,.T.);
#1322=FACE_OUTER_BOUND('',#1663,.T.);
#1323=FACE_OUTER_BOUND('',#1664,.T.);
#1324=FACE_OUTER_BOUND('',#1665,.T.);
#1325=FACE_OUTER_BOUND('',#1666,.T.);
#1326=FACE_OUTER_BOUND('',#1667,.T.);
#1327=FACE_OUTER_BOUND('',#1668,.T.);
#1328=FACE_OUTER_BOUND('',#1669,.T.);
#1329=FACE_OUTER_BOUND('',#1671,.T.);
#1330=FACE_OUTER_BOUND('',#1672,.T.);
#1331=FACE_OUTER_BOUND('',#1673,.T.);
#1332=FACE_OUTER_BOUND('',#1674,.T.);
#1333=FACE_OUTER_BOUND('',#1675,.T.);
#1334=FACE_OUTER_BOUND('',#1676,.T.);
#1335=FACE_OUTER_BOUND('',#1677,.T.);
#1336=FACE_OUTER_BOUND('',#1679,.T.);
#1337=FACE_OUTER_BOUND('',#1680,.T.);
#1661=EDGE_LOOP('',(#3686,#3687,#3688,#3689));
#1662=EDGE_LOOP('',(#3690,#3691,#3692,#3693));
#1663=EDGE_LOOP('',(#3694,#3695,#3696,#3697));
#1664=EDGE_LOOP('',(#3698,#3699,#3700,#3701));
#1665=EDGE_LOOP('',(#3702,#3703,#3704,#3705));
#1666=EDGE_LOOP('',(#3706,#3707,#3708,#3709));
#1667=EDGE_LOOP('',(#3710,#3711,#3712,#3713,#3714,#3715));
#1668=EDGE_LOOP('',(#3716,#3717,#3718,#3719,#3720,#3721));
#1669=EDGE_LOOP('',(#3722));
#1670=EDGE_LOOP('',(#3723));
#1671=EDGE_LOOP('',(#3724,#3725,#3726,#3727));
#1672=EDGE_LOOP('',(#3728));
#1673=EDGE_LOOP('',(#3729));
#1674=EDGE_LOOP('',(#3730,#3731,#3732,#3733));
#1675=EDGE_LOOP('',(#3734,#3735,#3736,#3737));
#1676=EDGE_LOOP('',(#3738,#3739,#3740,#3741));
#1677=EDGE_LOOP('',(#3742));
#1678=EDGE_LOOP('',(#3743));
#1679=EDGE_LOOP('',(#3744,#3745,#3746,#3747));
#1680=EDGE_LOOP('',(#3748,#3749,#3750,#3751));
#2027=CIRCLE('',#5493,0.4);
#2028=CIRCLE('',#5494,0.3933);
#2029=CIRCLE('',#5496,0.4);
#2030=CIRCLE('',#5499,0.6);
#2031=CIRCLE('',#5501,0.65);
#2032=CIRCLE('',#5503,0.65);
#2033=CIRCLE('',#5505,0.62);
#2034=CIRCLE('',#5507,0.42);
#2035=CIRCLE('',#5509,0.3933);
#2360=VERTEX_POINT('',#8051);
#2361=VERTEX_POINT('',#8052);
#2362=VERTEX_POINT('',#8054);
#2363=VERTEX_POINT('',#8056);
#2364=VERTEX_POINT('',#8060);
#2365=VERTEX_POINT('',#8062);
#2366=VERTEX_POINT('',#8066);
#2367=VERTEX_POINT('',#8068);
#2368=VERTEX_POINT('',#8072);
#2369=VERTEX_POINT('',#8074);
#2370=VERTEX_POINT('',#8078);
#2371=VERTEX_POINT('',#8080);
#2372=VERTEX_POINT('',#8089);
#2373=VERTEX_POINT('',#8091);
#2374=VERTEX_POINT('',#8094);
#2375=VERTEX_POINT('',#8099);
#2376=VERTEX_POINT('',#8102);
#2377=VERTEX_POINT('',#8106);
#2378=VERTEX_POINT('',#8110);
#2379=VERTEX_POINT('',#8114);
#2380=VERTEX_POINT('',#8117);
#2847=EDGE_CURVE('',#2360,#2361,#540,.T.);
#2848=EDGE_CURVE('',#2361,#2362,#541,.T.);
#2849=EDGE_CURVE('',#2362,#2363,#542,.T.);
#2850=EDGE_CURVE('',#2360,#2363,#543,.T.);
#2851=EDGE_CURVE('',#2361,#2364,#544,.T.);
#2852=EDGE_CURVE('',#2364,#2365,#545,.T.);
#2853=EDGE_CURVE('',#2365,#2362,#546,.T.);
#2854=EDGE_CURVE('',#2364,#2366,#547,.T.);
#2855=EDGE_CURVE('',#2366,#2367,#548,.T.);
#2856=EDGE_CURVE('',#2367,#2365,#549,.T.);
#2857=EDGE_CURVE('',#2366,#2368,#550,.T.);
#2858=EDGE_CURVE('',#2368,#2369,#551,.T.);
#2859=EDGE_CURVE('',#2369,#2367,#552,.T.);
#2860=EDGE_CURVE('',#2368,#2370,#553,.T.);
#2861=EDGE_CURVE('',#2370,#2371,#554,.T.);
#2862=EDGE_CURVE('',#2371,#2369,#555,.T.);
#2863=EDGE_CURVE('',#2370,#2360,#556,.T.);
#2864=EDGE_CURVE('',#2363,#2371,#557,.T.);
#2865=EDGE_CURVE('',#2372,#2372,#2027,.T.);
#2866=EDGE_CURVE('',#2373,#2373,#2028,.T.);
#2867=EDGE_CURVE('',#2372,#2374,#558,.T.);
#2868=EDGE_CURVE('',#2374,#2374,#2029,.T.);
#2869=EDGE_CURVE('',#2375,#2375,#2030,.T.);
#2870=EDGE_CURVE('',#2376,#2376,#2031,.T.);
#2871=EDGE_CURVE('',#2376,#2375,#559,.T.);
#2872=EDGE_CURVE('',#2377,#2377,#2032,.T.);
#2873=EDGE_CURVE('',#2377,#2376,#560,.T.);
#2874=EDGE_CURVE('',#2378,#2378,#2033,.T.);
#2875=EDGE_CURVE('',#2378,#2377,#561,.T.);
#2876=EDGE_CURVE('',#2379,#2379,#2034,.T.);
#2877=EDGE_CURVE('',#2380,#2380,#2035,.F.);
#2878=EDGE_CURVE('',#2380,#2379,#562,.T.);
#2879=EDGE_CURVE('',#2373,#2380,#563,.T.);
#3686=ORIENTED_EDGE('',*,*,#2847,.T.);
#3687=ORIENTED_EDGE('',*,*,#2848,.T.);
#3688=ORIENTED_EDGE('',*,*,#2849,.T.);
#3689=ORIENTED_EDGE('',*,*,#2850,.F.);
#3690=ORIENTED_EDGE('',*,*,#2851,.T.);
#3691=ORIENTED_EDGE('',*,*,#2852,.T.);
#3692=ORIENTED_EDGE('',*,*,#2853,.T.);
#3693=ORIENTED_EDGE('',*,*,#2848,.F.);
#3694=ORIENTED_EDGE('',*,*,#2854,.T.);
#3695=ORIENTED_EDGE('',*,*,#2855,.T.);
#3696=ORIENTED_EDGE('',*,*,#2856,.T.);
#3697=ORIENTED_EDGE('',*,*,#2852,.F.);
#3698=ORIENTED_EDGE('',*,*,#2857,.T.);
#3699=ORIENTED_EDGE('',*,*,#2858,.T.);
#3700=ORIENTED_EDGE('',*,*,#2859,.T.);
#3701=ORIENTED_EDGE('',*,*,#2855,.F.);
#3702=ORIENTED_EDGE('',*,*,#2860,.T.);
#3703=ORIENTED_EDGE('',*,*,#2861,.T.);
#3704=ORIENTED_EDGE('',*,*,#2862,.T.);
#3705=ORIENTED_EDGE('',*,*,#2858,.F.);
#3706=ORIENTED_EDGE('',*,*,#2863,.T.);
#3707=ORIENTED_EDGE('',*,*,#2850,.T.);
#3708=ORIENTED_EDGE('',*,*,#2864,.T.);
#3709=ORIENTED_EDGE('',*,*,#2861,.F.);
#3710=ORIENTED_EDGE('',*,*,#2863,.F.);
#3711=ORIENTED_EDGE('',*,*,#2860,.F.);
#3712=ORIENTED_EDGE('',*,*,#2857,.F.);
#3713=ORIENTED_EDGE('',*,*,#2854,.F.);
#3714=ORIENTED_EDGE('',*,*,#2851,.F.);
#3715=ORIENTED_EDGE('',*,*,#2847,.F.);
#3716=ORIENTED_EDGE('',*,*,#2864,.F.);
#3717=ORIENTED_EDGE('',*,*,#2849,.F.);
#3718=ORIENTED_EDGE('',*,*,#2853,.F.);
#3719=ORIENTED_EDGE('',*,*,#2856,.F.);
#3720=ORIENTED_EDGE('',*,*,#2859,.F.);
#3721=ORIENTED_EDGE('',*,*,#2862,.F.);
#3722=ORIENTED_EDGE('',*,*,#2865,.T.);
#3723=ORIENTED_EDGE('',*,*,#2866,.F.);
#3724=ORIENTED_EDGE('',*,*,#2865,.F.);
#3725=ORIENTED_EDGE('',*,*,#2867,.T.);
#3726=ORIENTED_EDGE('',*,*,#2868,.T.);
#3727=ORIENTED_EDGE('',*,*,#2867,.F.);
#3728=ORIENTED_EDGE('',*,*,#2868,.F.);
#3729=ORIENTED_EDGE('',*,*,#2869,.F.);
#3730=ORIENTED_EDGE('',*,*,#2870,.F.);
#3731=ORIENTED_EDGE('',*,*,#2871,.T.);
#3732=ORIENTED_EDGE('',*,*,#2869,.T.);
#3733=ORIENTED_EDGE('',*,*,#2871,.F.);
#3734=ORIENTED_EDGE('',*,*,#2872,.F.);
#3735=ORIENTED_EDGE('',*,*,#2873,.T.);
#3736=ORIENTED_EDGE('',*,*,#2870,.T.);
#3737=ORIENTED_EDGE('',*,*,#2873,.F.);
#3738=ORIENTED_EDGE('',*,*,#2874,.F.);
#3739=ORIENTED_EDGE('',*,*,#2875,.T.);
#3740=ORIENTED_EDGE('',*,*,#2872,.T.);
#3741=ORIENTED_EDGE('',*,*,#2875,.F.);
#3742=ORIENTED_EDGE('',*,*,#2874,.T.);
#3743=ORIENTED_EDGE('',*,*,#2876,.F.);
#3744=ORIENTED_EDGE('',*,*,#2877,.F.);
#3745=ORIENTED_EDGE('',*,*,#2878,.T.);
#3746=ORIENTED_EDGE('',*,*,#2876,.T.);
#3747=ORIENTED_EDGE('',*,*,#2878,.F.);
#3748=ORIENTED_EDGE('',*,*,#2866,.T.);
#3749=ORIENTED_EDGE('',*,*,#2879,.T.);
#3750=ORIENTED_EDGE('',*,*,#2877,.T.);
#3751=ORIENTED_EDGE('',*,*,#2879,.F.);
#4502=PLANE('',#5484);
#4503=PLANE('',#5485);
#4504=PLANE('',#5486);
#4505=PLANE('',#5487);
#4506=PLANE('',#5488);
#4507=PLANE('',#5489);
#4508=PLANE('',#5490);
#4509=PLANE('',#5491);
#4510=PLANE('',#5492);
#4511=PLANE('',#5497);
#4512=PLANE('',#5498);
#4513=PLANE('',#5506);
#4696=ADVANCED_FACE('',(#1320),#4502,.F.);
#4697=ADVANCED_FACE('',(#1321),#4503,.F.);
#4698=ADVANCED_FACE('',(#1322),#4504,.F.);
#4699=ADVANCED_FACE('',(#1323),#4505,.F.);
#4700=ADVANCED_FACE('',(#1324),#4506,.F.);
#4701=ADVANCED_FACE('',(#1325),#4507,.F.);
#4702=ADVANCED_FACE('',(#1326),#4508,.F.);
#4703=ADVANCED_FACE('',(#1327),#4509,.F.);
#4704=ADVANCED_FACE('',(#1328,#1159),#4510,.T.);
#4705=ADVANCED_FACE('',(#1329),#1048,.T.);
#4706=ADVANCED_FACE('',(#1330),#4511,.F.);
#4707=ADVANCED_FACE('',(#1331),#4512,.T.);
#4708=ADVANCED_FACE('',(#1332),#267,.T.);
#4709=ADVANCED_FACE('',(#1333),#1049,.T.);
#4710=ADVANCED_FACE('',(#1334),#268,.T.);
#4711=ADVANCED_FACE('',(#1335,#1160),#4513,.T.);
#4712=ADVANCED_FACE('',(#1336),#269,.T.);
#4713=ADVANCED_FACE('',(#1337),#1050,.T.);
#4899=CLOSED_SHELL('',(#4696,#4697,#4698,#4699,#4700,#4701,#4702,#4703));
#4900=CLOSED_SHELL('',(#4704,#4705,#4706,#4707,#4708,#4709,#4710,#4711,
#4712,#4713));
#5483=AXIS2_PLACEMENT_3D('',#8049,#6493,#6494);
#5484=AXIS2_PLACEMENT_3D('',#8050,#6495,#6496);
#5485=AXIS2_PLACEMENT_3D('',#8059,#6501,#6502);
#5486=AXIS2_PLACEMENT_3D('',#8065,#6506,#6507);
#5487=AXIS2_PLACEMENT_3D('',#8071,#6511,#6512);
#5488=AXIS2_PLACEMENT_3D('',#8077,#6516,#6517);
#5489=AXIS2_PLACEMENT_3D('',#8083,#6521,#6522);
#5490=AXIS2_PLACEMENT_3D('',#8086,#6525,#6526);
#5491=AXIS2_PLACEMENT_3D('',#8087,#6527,#6528);
#5492=AXIS2_PLACEMENT_3D('',#8088,#6529,#6530);
#5493=AXIS2_PLACEMENT_3D('',#8090,#6531,#6532);
#5494=AXIS2_PLACEMENT_3D('',#8092,#6533,#6534);
#5495=AXIS2_PLACEMENT_3D('',#8093,#6535,#6536);
#5496=AXIS2_PLACEMENT_3D('',#8096,#6538,#6539);
#5497=AXIS2_PLACEMENT_3D('',#8097,#6540,#6541);
#5498=AXIS2_PLACEMENT_3D('',#8098,#6542,#6543);
#5499=AXIS2_PLACEMENT_3D('',#8100,#6544,#6545);
#5500=AXIS2_PLACEMENT_3D('',#8101,#6546,#6547);
#5501=AXIS2_PLACEMENT_3D('',#8103,#6548,#6549);
#5502=AXIS2_PLACEMENT_3D('',#8105,#6551,#6552);
#5503=AXIS2_PLACEMENT_3D('',#8107,#6553,#6554);
#5504=AXIS2_PLACEMENT_3D('',#8109,#6556,#6557);
#5505=AXIS2_PLACEMENT_3D('',#8111,#6558,#6559);
#5506=AXIS2_PLACEMENT_3D('',#8113,#6561,#6562);
#5507=AXIS2_PLACEMENT_3D('',#8115,#6563,#6564);
#5508=AXIS2_PLACEMENT_3D('',#8116,#6565,#6566);
#5509=AXIS2_PLACEMENT_3D('',#8118,#6567,#6568);
#5510=AXIS2_PLACEMENT_3D('',#8120,#6570,#6571);
#6493=DIRECTION('axis',(0.,0.,1.));
#6494=DIRECTION('refdir',(1.,0.,0.));
#6495=DIRECTION('center_axis',(0.866025403784439,0.,-0.5));
#6496=DIRECTION('ref_axis',(0.5,0.,0.866025403784439));
#6497=DIRECTION('',(-0.5,0.,-0.866025403784439));
#6498=DIRECTION('',(0.,-1.,0.));
#6499=DIRECTION('',(0.5,0.,0.866025403784439));
#6500=DIRECTION('',(0.,-1.,0.));
#6501=DIRECTION('center_axis',(1.60246890531964E-16,0.,-1.));
#6502=DIRECTION('ref_axis',(1.,0.,1.60246890531964E-16));
#6503=DIRECTION('',(-1.,0.,-1.60246890531964E-16));
#6504=DIRECTION('',(0.,-1.,0.));
#6505=DIRECTION('',(1.,0.,1.60246890531964E-16));
#6506=DIRECTION('center_axis',(-0.866025403784439,0.,-0.5));
#6507=DIRECTION('ref_axis',(0.5,0.,-0.866025403784439));
#6508=DIRECTION('',(-0.5,0.,0.866025403784439));
#6509=DIRECTION('',(0.,-1.,0.));
#6510=DIRECTION('',(0.5,0.,-0.866025403784439));
#6511=DIRECTION('center_axis',(-0.866025403784439,0.,0.5));
#6512=DIRECTION('ref_axis',(-0.5,0.,-0.866025403784439));
#6513=DIRECTION('',(0.5,0.,0.866025403784439));
#6514=DIRECTION('',(0.,-1.,0.));
#6515=DIRECTION('',(-0.5,0.,-0.866025403784439));
#6516=DIRECTION('center_axis',(-1.60246890531964E-16,0.,1.));
#6517=DIRECTION('ref_axis',(-1.,0.,-1.60246890531964E-16));
#6518=DIRECTION('',(1.,0.,1.60246890531964E-16));
#6519=DIRECTION('',(0.,-1.,0.));
#6520=DIRECTION('',(-1.,0.,-1.60246890531964E-16));
#6521=DIRECTION('center_axis',(0.866025403784439,0.,0.5));
#6522=DIRECTION('ref_axis',(-0.5,0.,0.866025403784439));
#6523=DIRECTION('',(0.5,0.,-0.866025403784439));
#6524=DIRECTION('',(-0.5,0.,0.866025403784439));
#6525=DIRECTION('center_axis',(0.,1.,0.));
#6526=DIRECTION('ref_axis',(1.,0.,0.));
#6527=DIRECTION('center_axis',(0.,-1.,0.));
#6528=DIRECTION('ref_axis',(0.,0.,-1.));
#6529=DIRECTION('center_axis',(0.,1.,0.));
#6530=DIRECTION('ref_axis',(1.,0.,0.));
#6531=DIRECTION('center_axis',(0.,1.,0.));
#6532=DIRECTION('ref_axis',(1.,0.,0.));
#6533=DIRECTION('center_axis',(0.,1.,0.));
#6534=DIRECTION('ref_axis',(1.,0.,0.));
#6535=DIRECTION('center_axis',(0.,1.,0.));
#6536=DIRECTION('ref_axis',(1.,0.,0.));
#6537=DIRECTION('',(0.,-1.,0.));
#6538=DIRECTION('center_axis',(0.,1.,0.));
#6539=DIRECTION('ref_axis',(1.,0.,0.));
#6540=DIRECTION('center_axis',(0.,1.,0.));
#6541=DIRECTION('ref_axis',(1.,0.,0.));
#6542=DIRECTION('center_axis',(0.,1.,0.));
#6543=DIRECTION('ref_axis',(0.,0.,1.));
#6544=DIRECTION('center_axis',(0.,-1.,0.));
#6545=DIRECTION('ref_axis',(1.,0.,0.));
#6546=DIRECTION('center_axis',(0.,-1.,0.));
#6547=DIRECTION('ref_axis',(1.,0.,0.));
#6548=DIRECTION('center_axis',(0.,-1.,0.));
#6549=DIRECTION('ref_axis',(1.,0.,0.));
#6550=DIRECTION('',(0.707106781186548,0.707106781186547,8.65956056235493E-17));
#6551=DIRECTION('center_axis',(0.,-1.,0.));
#6552=DIRECTION('ref_axis',(1.,0.,0.));
#6553=DIRECTION('center_axis',(0.,-1.,0.));
#6554=DIRECTION('ref_axis',(1.,0.,0.));
#6555=DIRECTION('',(0.,1.,0.));
#6556=DIRECTION('center_axis',(0.,1.,0.));
#6557=DIRECTION('ref_axis',(1.,0.,0.));
#6558=DIRECTION('center_axis',(0.,-1.,0.));
#6559=DIRECTION('ref_axis',(1.,0.,0.));
#6560=DIRECTION('',(-0.707106781186548,0.707106781186547,-8.65956056235494E-17));
#6561=DIRECTION('center_axis',(0.,-1.,0.));
#6562=DIRECTION('ref_axis',(0.,0.,-1.));
#6563=DIRECTION('center_axis',(0.,-1.,0.));
#6564=DIRECTION('ref_axis',(1.,0.,0.));
#6565=DIRECTION('center_axis',(0.,1.,0.));
#6566=DIRECTION('ref_axis',(1.,0.,0.));
#6567=DIRECTION('center_axis',(0.,1.,0.));
#6568=DIRECTION('ref_axis',(1.,0.,0.));
#6569=DIRECTION('',(-0.447213595499958,0.894427190999916,-5.47678698264203E-17));
#6570=DIRECTION('center_axis',(0.,-1.,0.));
#6571=DIRECTION('ref_axis',(1.,0.,0.));
#6572=DIRECTION('',(0.,1.,0.));
#8049=CARTESIAN_POINT('',(0.,0.,0.));
#8050=CARTESIAN_POINT('Origin',(0.173205080756888,-0.8,-0.3));
#8051=CARTESIAN_POINT('',(0.346410161513775,-0.8,0.));
#8052=CARTESIAN_POINT('',(0.173205080756888,-0.8,-0.3));
#8053=CARTESIAN_POINT('',(0.346410161513775,-0.8,0.));
#8054=CARTESIAN_POINT('',(0.173205080756888,-1.28,-0.3));
#8055=CARTESIAN_POINT('',(0.173205080756888,-0.8,-0.3));
#8056=CARTESIAN_POINT('',(0.346410161513775,-1.28,0.));
#8057=CARTESIAN_POINT('',(0.346410161513775,-1.28,0.));
#8058=CARTESIAN_POINT('',(0.346410161513775,-0.8,0.));
#8059=CARTESIAN_POINT('Origin',(-0.173205080756888,-0.8,-0.3));
#8060=CARTESIAN_POINT('',(-0.173205080756888,-0.8,-0.3));
#8061=CARTESIAN_POINT('',(0.173205080756888,-0.8,-0.3));
#8062=CARTESIAN_POINT('',(-0.173205080756888,-1.28,-0.3));
#8063=CARTESIAN_POINT('',(-0.173205080756888,-0.8,-0.3));
#8064=CARTESIAN_POINT('',(0.173205080756888,-1.28,-0.3));
#8065=CARTESIAN_POINT('Origin',(-0.346410161513775,-0.8,-5.55111512312578E-17));
#8066=CARTESIAN_POINT('',(-0.346410161513775,-0.8,-4.24230095489963E-17));
#8067=CARTESIAN_POINT('',(-0.173205080756888,-0.8,-0.3));
#8068=CARTESIAN_POINT('',(-0.346410161513775,-1.28,-5.55111512312578E-17));
#8069=CARTESIAN_POINT('',(-0.346410161513775,-0.8,-4.24230095489963E-17));
#8070=CARTESIAN_POINT('',(-0.173205080756888,-1.28,-0.3));
#8071=CARTESIAN_POINT('Origin',(-0.173205080756888,-0.8,0.3));
#8072=CARTESIAN_POINT('',(-0.173205080756888,-0.8,0.3));
#8073=CARTESIAN_POINT('',(-0.346410161513775,-0.8,-4.24230095489963E-17));
#8074=CARTESIAN_POINT('',(-0.173205080756888,-1.28,0.3));
#8075=CARTESIAN_POINT('',(-0.173205080756888,-0.8,0.3));
#8076=CARTESIAN_POINT('',(-0.346410161513775,-1.28,-4.24230095489963E-17));
#8077=CARTESIAN_POINT('Origin',(0.173205080756888,-0.8,0.3));
#8078=CARTESIAN_POINT('',(0.173205080756888,-0.8,0.3));
#8079=CARTESIAN_POINT('',(-0.173205080756888,-0.8,0.3));
#8080=CARTESIAN_POINT('',(0.173205080756888,-1.28,0.3));
#8081=CARTESIAN_POINT('',(0.173205080756888,-0.8,0.3));
#8082=CARTESIAN_POINT('',(-0.173205080756888,-1.28,0.3));
#8083=CARTESIAN_POINT('Origin',(0.346410161513775,-0.8,0.));
#8084=CARTESIAN_POINT('',(0.173205080756888,-0.8,0.3));
#8085=CARTESIAN_POINT('',(0.173205080756888,-1.28,0.3));
#8086=CARTESIAN_POINT('Origin',(0.,-0.8,-5.55111512312578E-17));
#8087=CARTESIAN_POINT('Origin',(0.,-1.28,-5.55111512312578E-17));
#8088=CARTESIAN_POINT('Origin',(0.,-2.9,0.));
#8089=CARTESIAN_POINT('',(-0.4,-2.9,4.89858719658941E-17));
#8090=CARTESIAN_POINT('Origin',(0.,-2.9,0.));
#8091=CARTESIAN_POINT('',(-0.3933,-2.9,4.81653586104654E-17));
#8092=CARTESIAN_POINT('Origin',(0.,-2.9,0.));
#8093=CARTESIAN_POINT('Origin',(0.,-7.5,0.));
#8094=CARTESIAN_POINT('',(-0.4,-7.5,4.89858719658941E-17));
#8095=CARTESIAN_POINT('',(-0.4,-7.5,4.89858719658941E-17));
#8096=CARTESIAN_POINT('Origin',(0.,-7.5,0.));
#8097=CARTESIAN_POINT('Origin',(0.,-7.5,0.));
#8098=CARTESIAN_POINT('Origin',(0.6,0.8,0.));
#8099=CARTESIAN_POINT('',(-0.6,0.8,-7.34788079488412E-17));
#8100=CARTESIAN_POINT('Origin',(0.,0.8,0.));
#8101=CARTESIAN_POINT('Origin',(0.,0.775,0.));
#8102=CARTESIAN_POINT('',(-0.65,0.75,-7.9602041944578E-17));
#8103=CARTESIAN_POINT('Origin',(0.,0.75,0.));
#8104=CARTESIAN_POINT('',(-0.625,0.775,-7.65404249467096E-17));
#8105=CARTESIAN_POINT('Origin',(0.,0.39,0.));
#8106=CARTESIAN_POINT('',(-0.65,0.0299999999999998,-7.9602041944578E-17));
#8107=CARTESIAN_POINT('Origin',(0.,0.0299999999999998,0.));
#8108=CARTESIAN_POINT('',(-0.65,0.39,-7.9602041944578E-17));
#8109=CARTESIAN_POINT('Origin',(0.,0.0150000000000001,0.));
#8110=CARTESIAN_POINT('',(-0.62,5.89805981832114E-17,-7.59281015471359E-17));
#8111=CARTESIAN_POINT('Origin',(0.,0.,0.));
#8112=CARTESIAN_POINT('',(-0.635,0.0150000000000001,-7.77650717458569E-17));
#8113=CARTESIAN_POINT('Origin',(0.42,0.,0.));
#8114=CARTESIAN_POINT('',(-0.42,-3.46944695195361E-18,-5.14351655641888E-17));
#8115=CARTESIAN_POINT('Origin',(0.,0.,0.));
#8116=CARTESIAN_POINT('Origin',(0.,-0.02,0.));
#8117=CARTESIAN_POINT('',(-0.3933,-0.0534000000000001,4.81653586104654E-17));
#8118=CARTESIAN_POINT('Origin',(0.,-0.0534000000000001,0.));
#8119=CARTESIAN_POINT('',(-0.41,-0.02,-5.02105187650415E-17));
#8120=CARTESIAN_POINT('Origin',(0.,-1.48,0.));
#8121=CARTESIAN_POINT('',(-0.3933,-1.48,-4.81653586104654E-17));
#9332=UNCERTAINTY_MEASURE_WITH_UNIT(LENGTH_MEASURE(0.001),#9392,
'DISTANCE_ACCURACY_VALUE',
'Maximum model space distance between geometric entities at asserted c
onnectivities');
#9354=UNCERTAINTY_MEASURE_WITH_UNIT(LENGTH_MEASURE(0.001),#9392,
'DISTANCE_ACCURACY_VALUE',
'Maximum model space distance between geometric entities at asserted c
onnectivities');
#9369=(
GEOMETRIC_REPRESENTATION_CONTEXT(3)
GLOBAL_UNCERTAINTY_ASSIGNED_CONTEXT((#9332))
GLOBAL_UNIT_ASSIGNED_CONTEXT((#9392,#9394,#9395))
REPRESENTATION_CONTEXT('','3D')
);
#9391=(
GEOMETRIC_REPRESENTATION_CONTEXT(3)
GLOBAL_UNCERTAINTY_ASSIGNED_CONTEXT((#9354))
GLOBAL_UNIT_ASSIGNED_CONTEXT((#9392,#9394,#9395))
REPRESENTATION_CONTEXT('','3D')
);
#9392=(
LENGTH_UNIT()
NAMED_UNIT(*)
SI_UNIT(.CENTI.,.METRE.)
);
#9394=(
NAMED_UNIT(*)
PLANE_ANGLE_UNIT()
SI_UNIT($,.RADIAN.)
);
#9395=(
NAMED_UNIT(*)
SI_UNIT($,.STERADIAN.)
SOLID_ANGLE_UNIT()
);
#9410=SHAPE_DEFINITION_REPRESENTATION(#9446,#9534);
#9446=PRODUCT_DEFINITION_SHAPE('',$,#9571);
#9534=SHAPE_REPRESENTATION('',(#5483),#9369);
#9556=PRODUCT_DEFINITION_CONTEXT('part definition',#9666,'design');
#9571=PRODUCT_DEFINITION('M8x75 cross bolt','M8x75 cross bolt',#9607,#9556);
#9607=PRODUCT_DEFINITION_FORMATION('',$,#9682);
#9666=APPLICATION_CONTEXT(
'Core Data for Automotive Mechanical Design Process');
#9667=PRODUCT_CONTEXT('part definition',#9666,'mechanical');
#9682=PRODUCT('M8x75 cross bolt','M8x75 cross bolt','M8x75 cross bolt',
(#9667));
#9760=COLOUR_RGB('Black',0.12,0.14,0.17);
#9761=FILL_AREA_STYLE_COLOUR('',#9760);
#9762=FILL_AREA_STYLE('',(#9761));
#9763=SURFACE_STYLE_FILL_AREA(#9762);
#9764=SURFACE_SIDE_STYLE('',(#9763));
#9765=SURFACE_STYLE_USAGE(.BOTH.,#9764);
#9766=PRESENTATION_STYLE_ASSIGNMENT((#9765));
ENDSEC;
END-ISO-10303-21;
